ISO-10303-21;
HEADER;
/* Generated by software containing ST-Developer
 * from STEP Tools, Inc. (www.steptools.com) 
 */

FILE_DESCRIPTION(
/* description */ ('Belt conveyor head drive unit'),
/* implementation_level */ '2;1');

FILE_NAME(
/* name */ 'Cap Screw - M5x20.step',
/* time_stamp */ '2026-10-28T03:26:19-07:00',
/* author */ (''),
/* organization */ (''),
/* preprocessor_version */ 'ST-DEVELOPER v20.2',
/* originating_system */ 'Autodesk Translation Framework v15.17.0.0',
/* authorisation */ '');

FILE_SCHEMA (('AUTOMOTIVE_DESIGN { 1 0 10303 214 3 1 1 }'));
ENDSEC;

DATA;
#10=MECHANICAL_DESIGN_GEOMETRIC_PRESENTATION_REPRESENTATION('',(#900),#27069);
#12=ORIENTED_CLOSED_SHELL('',*,#13767,.F.);
#17=BREP_WITH_VOIDS('Body1',#13766,(#12));
#689=CONICAL_SURFACE('',#15484,0.4,0.785398163397448);
#690=CONICAL_SURFACE('',#15488,0.41,0.785398163397448);
#691=CONICAL_SURFACE('',#15492,0.26,0.463647609000806);
#692=CONICAL_SURFACE('',#15496,0.225,0.785398163397448);
#747=SHAPE_REPRESENTATION_RELATIONSHIP('SRR','None',#27393,#816);
#816=ADVANCED_BREP_SHAPE_REPRESENTATION('',(#17),#27035);
#900=STYLED_ITEM('',(#27804),#17);
#1171=FACE_BOUND('',#3017,.T.);
#1482=PLANE('',#15482);
#1483=PLANE('',#15490);
#1484=PLANE('',#15498);
#1485=PLANE('',#15499);
#1486=PLANE('',#15500);
#1487=PLANE('',#15501);
#1488=PLANE('',#15502);
#1489=PLANE('',#15503);
#1490=PLANE('',#15504);
#1491=PLANE('',#15505);
#1492=PLANE('',#15506);
#2053=FACE_OUTER_BOUND('',#3012,.T.);
#2054=FACE_OUTER_BOUND('',#3013,.T.);
#2055=FACE_OUTER_BOUND('',#3014,.T.);
#2056=FACE_OUTER_BOUND('',#3015,.T.);
#2057=FACE_OUTER_BOUND('',#3016,.T.);
#2058=FACE_OUTER_BOUND('',#3018,.T.);
#2059=FACE_OUTER_BOUND('',#3019,.T.);
#2060=FACE_OUTER_BOUND('',#3020,.T.);
#2061=FACE_OUTER_BOUND('',#3021,.T.);
#2062=FACE_OUTER_BOUND('',#3022,.T.);
#2063=FACE_OUTER_BOUND('',#3023,.T.);
#2064=FACE_OUTER_BOUND('',#3024,.T.);
#2065=FACE_OUTER_BOUND('',#3025,.T.);
#2066=FACE_OUTER_BOUND('',#3026,.T.);
#2067=FACE_OUTER_BOUND('',#3027,.T.);
#2068=FACE_OUTER_BOUND('',#3028,.T.);
#2069=FACE_OUTER_BOUND('',#3029,.T.);
#3012=EDGE_LOOP('',(#10752));
#3013=EDGE_LOOP('',(#10753,#10754,#10755,#10756));
#3014=EDGE_LOOP('',(#10757,#10758,#10759,#10760));
#3015=EDGE_LOOP('',(#10761,#10762,#10763,#10764));
#3016=EDGE_LOOP('',(#10765));
#3017=EDGE_LOOP('',(#10766));
#3018=EDGE_LOOP('',(#10767,#10768,#10769,#10770));
#3019=EDGE_LOOP('',(#10771,#10772,#10773,#10774));
#3020=EDGE_LOOP('',(#10775,#10776,#10777,#10778));
#3021=EDGE_LOOP('',(#10779));
#3022=EDGE_LOOP('',(#10780,#10781,#10782,#10783));
#3023=EDGE_LOOP('',(#10784,#10785,#10786,#10787));
#3024=EDGE_LOOP('',(#10788,#10789,#10790,#10791));
#3025=EDGE_LOOP('',(#10792,#10793,#10794,#10795));
#3026=EDGE_LOOP('',(#10796,#10797,#10798,#10799));
#3027=EDGE_LOOP('',(#10800,#10801,#10802,#10803));
#3028=EDGE_LOOP('',(#10804,#10805,#10806,#10807,#10808,#10809));
#3029=EDGE_LOOP('',(#10810,#10811,#10812,#10813,#10814,#10815));
#3916=LINE('',#23592,#4708);
#3917=LINE('',#23596,#4709);
#3918=LINE('',#23600,#4710);
#3919=LINE('',#23607,#4711);
#3920=LINE('',#23611,#4712);
#3921=LINE('',#23615,#4713);
#3922=LINE('',#23620,#4714);
#3923=LINE('',#23622,#4715);
#3924=LINE('',#23624,#4716);
#3925=LINE('',#23625,#4717);
#3926=LINE('',#23628,#4718);
#3927=LINE('',#23630,#4719);
#3928=LINE('',#23631,#4720);
#3929=LINE('',#23634,#4721);
#3930=LINE('',#23636,#4722);
#3931=LINE('',#23637,#4723);
#3932=LINE('',#23640,#4724);
#3933=LINE('',#23642,#4725);
#3934=LINE('',#23643,#4726);
#3935=LINE('',#23646,#4727);
#3936=LINE('',#23648,#4728);
#3937=LINE('',#23649,#4729);
#3938=LINE('',#23651,#4730);
#3939=LINE('',#23652,#4731);
#4708=VECTOR('',#18700,0.4);
#4709=VECTOR('',#18705,0.425);
#4710=VECTOR('',#18710,0.41);
#4711=VECTOR('',#18719,0.26);
#4712=VECTOR('',#18724,0.25);
#4713=VECTOR('',#18729,0.225);
#4714=VECTOR('',#18734,1.);
#4715=VECTOR('',#18735,1.);
#4716=VECTOR('',#18736,1.);
#4717=VECTOR('',#18737,1.);
#4718=VECTOR('',#18740,1.);
#4719=VECTOR('',#18741,1.);
#4720=VECTOR('',#18742,1.);
#4721=VECTOR('',#18745,1.);
#4722=VECTOR('',#18746,1.);
#4723=VECTOR('',#18747,1.);
#4724=VECTOR('',#18750,1.);
#4725=VECTOR('',#18751,1.);
#4726=VECTOR('',#18752,1.);
#4727=VECTOR('',#18755,1.);
#4728=VECTOR('',#18756,1.);
#4729=VECTOR('',#18757,1.);
#4730=VECTOR('',#18760,1.);
#4731=VECTOR('',#18761,1.);
#5529=CIRCLE('',#15483,0.375);
#5530=CIRCLE('',#15485,0.425);
#5531=CIRCLE('',#15487,0.425);
#5532=CIRCLE('',#15489,0.395);
#5533=CIRCLE('',#15491,0.27);
#5534=CIRCLE('',#15493,0.24505);
#5535=CIRCLE('',#15495,0.24505);
#5536=CIRCLE('',#15497,0.2);
#6567=VERTEX_POINT('',#23587);
#6568=VERTEX_POINT('',#23590);
#6569=VERTEX_POINT('',#23594);
#6570=VERTEX_POINT('',#23598);
#6571=VERTEX_POINT('',#23602);
#6572=VERTEX_POINT('',#23605);
#6573=VERTEX_POINT('',#23609);
#6574=VERTEX_POINT('',#23613);
#6575=VERTEX_POINT('',#23618);
#6576=VERTEX_POINT('',#23619);
#6577=VERTEX_POINT('',#23621);
#6578=VERTEX_POINT('',#23623);
#6579=VERTEX_POINT('',#23627);
#6580=VERTEX_POINT('',#23629);
#6581=VERTEX_POINT('',#23633);
#6582=VERTEX_POINT('',#23635);
#6583=VERTEX_POINT('',#23639);
#6584=VERTEX_POINT('',#23641);
#6585=VERTEX_POINT('',#23645);
#6586=VERTEX_POINT('',#23647);
#8068=EDGE_CURVE('',#6567,#6567,#5529,.T.);
#8069=EDGE_CURVE('',#6568,#6568,#5530,.T.);
#8070=EDGE_CURVE('',#6568,#6567,#3916,.T.);
#8071=EDGE_CURVE('',#6569,#6569,#5531,.T.);
#8072=EDGE_CURVE('',#6569,#6568,#3917,.T.);
#8073=EDGE_CURVE('',#6570,#6570,#5532,.T.);
#8074=EDGE_CURVE('',#6570,#6569,#3918,.T.);
#8075=EDGE_CURVE('',#6571,#6571,#5533,.T.);
#8076=EDGE_CURVE('',#6572,#6572,#5534,.F.);
#8077=EDGE_CURVE('',#6572,#6571,#3919,.T.);
#8078=EDGE_CURVE('',#6573,#6573,#5535,.F.);
#8079=EDGE_CURVE('',#6573,#6572,#3920,.T.);
#8080=EDGE_CURVE('',#6574,#6574,#5536,.T.);
#8081=EDGE_CURVE('',#6574,#6573,#3921,.T.);
#8082=EDGE_CURVE('',#6575,#6576,#3922,.T.);
#8083=EDGE_CURVE('',#6576,#6577,#3923,.T.);
#8084=EDGE_CURVE('',#6577,#6578,#3924,.T.);
#8085=EDGE_CURVE('',#6575,#6578,#3925,.T.);
#8086=EDGE_CURVE('',#6576,#6579,#3926,.T.);
#8087=EDGE_CURVE('',#6579,#6580,#3927,.T.);
#8088=EDGE_CURVE('',#6580,#6577,#3928,.T.);
#8089=EDGE_CURVE('',#6579,#6581,#3929,.T.);
#8090=EDGE_CURVE('',#6581,#6582,#3930,.T.);
#8091=EDGE_CURVE('',#6582,#6580,#3931,.T.);
#8092=EDGE_CURVE('',#6581,#6583,#3932,.T.);
#8093=EDGE_CURVE('',#6583,#6584,#3933,.T.);
#8094=EDGE_CURVE('',#6584,#6582,#3934,.T.);
#8095=EDGE_CURVE('',#6583,#6585,#3935,.T.);
#8096=EDGE_CURVE('',#6585,#6586,#3936,.T.);
#8097=EDGE_CURVE('',#6586,#6584,#3937,.T.);
#8098=EDGE_CURVE('',#6585,#6575,#3938,.T.);
#8099=EDGE_CURVE('',#6578,#6586,#3939,.T.);
#10752=ORIENTED_EDGE('',*,*,#8068,.F.);
#10753=ORIENTED_EDGE('',*,*,#8069,.F.);
#10754=ORIENTED_EDGE('',*,*,#8070,.T.);
#10755=ORIENTED_EDGE('',*,*,#8068,.T.);
#10756=ORIENTED_EDGE('',*,*,#8070,.F.);
#10757=ORIENTED_EDGE('',*,*,#8071,.F.);
#10758=ORIENTED_EDGE('',*,*,#8072,.T.);
#10759=ORIENTED_EDGE('',*,*,#8069,.T.);
#10760=ORIENTED_EDGE('',*,*,#8072,.F.);
#10761=ORIENTED_EDGE('',*,*,#8073,.F.);
#10762=ORIENTED_EDGE('',*,*,#8074,.T.);
#10763=ORIENTED_EDGE('',*,*,#8071,.T.);
#10764=ORIENTED_EDGE('',*,*,#8074,.F.);
#10765=ORIENTED_EDGE('',*,*,#8073,.T.);
#10766=ORIENTED_EDGE('',*,*,#8075,.F.);
#10767=ORIENTED_EDGE('',*,*,#8076,.F.);
#10768=ORIENTED_EDGE('',*,*,#8077,.T.);
#10769=ORIENTED_EDGE('',*,*,#8075,.T.);
#10770=ORIENTED_EDGE('',*,*,#8077,.F.);
#10771=ORIENTED_EDGE('',*,*,#8078,.F.);
#10772=ORIENTED_EDGE('',*,*,#8079,.T.);
#10773=ORIENTED_EDGE('',*,*,#8076,.T.);
#10774=ORIENTED_EDGE('',*,*,#8079,.F.);
#10775=ORIENTED_EDGE('',*,*,#8080,.F.);
#10776=ORIENTED_EDGE('',*,*,#8081,.T.);
#10777=ORIENTED_EDGE('',*,*,#8078,.T.);
#10778=ORIENTED_EDGE('',*,*,#8081,.F.);
#10779=ORIENTED_EDGE('',*,*,#8080,.T.);
#10780=ORIENTED_EDGE('',*,*,#8082,.T.);
#10781=ORIENTED_EDGE('',*,*,#8083,.T.);
#10782=ORIENTED_EDGE('',*,*,#8084,.T.);
#10783=ORIENTED_EDGE('',*,*,#8085,.F.);
#10784=ORIENTED_EDGE('',*,*,#8086,.T.);
#10785=ORIENTED_EDGE('',*,*,#8087,.T.);
#10786=ORIENTED_EDGE('',*,*,#8088,.T.);
#10787=ORIENTED_EDGE('',*,*,#8083,.F.);
#10788=ORIENTED_EDGE('',*,*,#8089,.T.);
#10789=ORIENTED_EDGE('',*,*,#8090,.T.);
#10790=ORIENTED_EDGE('',*,*,#8091,.T.);
#10791=ORIENTED_EDGE('',*,*,#8087,.F.);
#10792=ORIENTED_EDGE('',*,*,#8092,.T.);
#10793=ORIENTED_EDGE('',*,*,#8093,.T.);
#10794=ORIENTED_EDGE('',*,*,#8094,.T.);
#10795=ORIENTED_EDGE('',*,*,#8090,.F.);
#10796=ORIENTED_EDGE('',*,*,#8095,.T.);
#10797=ORIENTED_EDGE('',*,*,#8096,.T.);
#10798=ORIENTED_EDGE('',*,*,#8097,.T.);
#10799=ORIENTED_EDGE('',*,*,#8093,.F.);
#10800=ORIENTED_EDGE('',*,*,#8098,.T.);
#10801=ORIENTED_EDGE('',*,*,#8085,.T.);
#10802=ORIENTED_EDGE('',*,*,#8099,.T.);
#10803=ORIENTED_EDGE('',*,*,#8096,.F.);
#10804=ORIENTED_EDGE('',*,*,#8098,.F.);
#10805=ORIENTED_EDGE('',*,*,#8095,.F.);
#10806=ORIENTED_EDGE('',*,*,#8092,.F.);
#10807=ORIENTED_EDGE('',*,*,#8089,.F.);
#10808=ORIENTED_EDGE('',*,*,#8086,.F.);
#10809=ORIENTED_EDGE('',*,*,#8082,.F.);
#10810=ORIENTED_EDGE('',*,*,#8099,.F.);
#10811=ORIENTED_EDGE('',*,*,#8084,.F.);
#10812=ORIENTED_EDGE('',*,*,#8088,.F.);
#10813=ORIENTED_EDGE('',*,*,#8091,.F.);
#10814=ORIENTED_EDGE('',*,*,#8094,.F.);
#10815=ORIENTED_EDGE('',*,*,#8097,.F.);
#12701=CYLINDRICAL_SURFACE('',#15486,0.425);
#12702=CYLINDRICAL_SURFACE('',#15494,0.24505);
#13332=ADVANCED_FACE('',(#2053),#1482,.T.);
#13333=ADVANCED_FACE('',(#2054),#689,.T.);
#13334=ADVANCED_FACE('',(#2055),#12701,.T.);
#13335=ADVANCED_FACE('',(#2056),#690,.T.);
#13336=ADVANCED_FACE('',(#2057,#1171),#1483,.T.);
#13337=ADVANCED_FACE('',(#2058),#691,.T.);
#13338=ADVANCED_FACE('',(#2059),#12702,.T.);
#13339=ADVANCED_FACE('',(#2060),#692,.T.);
#13340=ADVANCED_FACE('',(#2061),#1484,.T.);
#13341=ADVANCED_FACE('',(#2062),#1485,.F.);
#13342=ADVANCED_FACE('',(#2063),#1486,.F.);
#13343=ADVANCED_FACE('',(#2064),#1487,.F.);
#13344=ADVANCED_FACE('',(#2065),#1488,.F.);
#13345=ADVANCED_FACE('',(#2066),#1489,.F.);
#13346=ADVANCED_FACE('',(#2067),#1490,.F.);
#13347=ADVANCED_FACE('',(#2068),#1491,.F.);
#13348=ADVANCED_FACE('',(#2069),#1492,.F.);
#13766=CLOSED_SHELL('',(#13332,#13333,#13334,#13335,#13336,#13337,#13338,
#13339,#13340));
#13767=CLOSED_SHELL('',(#13341,#13342,#13343,#13344,#13345,#13346,#13347,
#13348));
#15481=AXIS2_PLACEMENT_3D('',#23585,#18690,#18691);
#15482=AXIS2_PLACEMENT_3D('',#23586,#18692,#18693);
#15483=AXIS2_PLACEMENT_3D('',#23588,#18694,#18695);
#15484=AXIS2_PLACEMENT_3D('',#23589,#18696,#18697);
#15485=AXIS2_PLACEMENT_3D('',#23591,#18698,#18699);
#15486=AXIS2_PLACEMENT_3D('',#23593,#18701,#18702);
#15487=AXIS2_PLACEMENT_3D('',#23595,#18703,#18704);
#15488=AXIS2_PLACEMENT_3D('',#23597,#18706,#18707);
#15489=AXIS2_PLACEMENT_3D('',#23599,#18708,#18709);
#15490=AXIS2_PLACEMENT_3D('',#23601,#18711,#18712);
#15491=AXIS2_PLACEMENT_3D('',#23603,#18713,#18714);
#15492=AXIS2_PLACEMENT_3D('',#23604,#18715,#18716);
#15493=AXIS2_PLACEMENT_3D('',#23606,#18717,#18718);
#15494=AXIS2_PLACEMENT_3D('',#23608,#18720,#18721);
#15495=AXIS2_PLACEMENT_3D('',#23610,#18722,#18723);
#15496=AXIS2_PLACEMENT_3D('',#23612,#18725,#18726);
#15497=AXIS2_PLACEMENT_3D('',#23614,#18727,#18728);
#15498=AXIS2_PLACEMENT_3D('',#23616,#18730,#18731);
#15499=AXIS2_PLACEMENT_3D('',#23617,#18732,#18733);
#15500=AXIS2_PLACEMENT_3D('',#23626,#18738,#18739);
#15501=AXIS2_PLACEMENT_3D('',#23632,#18743,#18744);
#15502=AXIS2_PLACEMENT_3D('',#23638,#18748,#18749);
#15503=AXIS2_PLACEMENT_3D('',#23644,#18753,#18754);
#15504=AXIS2_PLACEMENT_3D('',#23650,#18758,#18759);
#15505=AXIS2_PLACEMENT_3D('',#23653,#18762,#18763);
#15506=AXIS2_PLACEMENT_3D('',#23654,#18764,#18765);
#18690=DIRECTION('axis',(0.,0.,1.));
#18691=DIRECTION('refdir',(1.,0.,0.));
#18692=DIRECTION('center_axis',(0.,1.,0.));
#18693=DIRECTION('ref_axis',(0.,0.,1.));
#18694=DIRECTION('center_axis',(0.,-1.,0.));
#18695=DIRECTION('ref_axis',(1.,0.,0.));
#18696=DIRECTION('center_axis',(0.,-1.,0.));
#18697=DIRECTION('ref_axis',(1.,0.,0.));
#18698=DIRECTION('center_axis',(0.,-1.,0.));
#18699=DIRECTION('ref_axis',(1.,0.,0.));
#18700=DIRECTION('',(0.707106781186548,0.707106781186547,8.65956056235493E-17));
#18701=DIRECTION('center_axis',(0.,-1.,0.));
#18702=DIRECTION('ref_axis',(1.,0.,0.));
#18703=DIRECTION('center_axis',(0.,-1.,0.));
#18704=DIRECTION('ref_axis',(1.,0.,0.));
#18705=DIRECTION('',(0.,1.,0.));
#18706=DIRECTION('center_axis',(0.,1.,0.));
#18707=DIRECTION('ref_axis',(1.,0.,0.));
#18708=DIRECTION('center_axis',(0.,-1.,0.));
#18709=DIRECTION('ref_axis',(1.,0.,0.));
#18710=DIRECTION('',(-0.707106781186547,0.707106781186548,-8.65956056235493E-17));
#18711=DIRECTION('center_axis',(0.,-1.,0.));
#18712=DIRECTION('ref_axis',(0.,0.,-1.));
#18713=DIRECTION('center_axis',(0.,-1.,0.));
#18714=DIRECTION('ref_axis',(1.,0.,0.));
#18715=DIRECTION('center_axis',(0.,1.,0.));
#18716=DIRECTION('ref_axis',(1.,0.,0.));
#18717=DIRECTION('center_axis',(0.,1.,0.));
#18718=DIRECTION('ref_axis',(1.,0.,0.));
#18719=DIRECTION('',(-0.447213595499958,0.894427190999916,-5.47678698264203E-17));
#18720=DIRECTION('center_axis',(0.,-1.,0.));
#18721=DIRECTION('ref_axis',(1.,0.,0.));
#18722=DIRECTION('center_axis',(0.,1.,0.));
#18723=DIRECTION('ref_axis',(1.,0.,0.));
#18724=DIRECTION('',(0.,1.,0.));
#18725=DIRECTION('center_axis',(0.,1.,0.));
#18726=DIRECTION('ref_axis',(1.,0.,0.));
#18727=DIRECTION('center_axis',(0.,-1.,0.));
#18728=DIRECTION('ref_axis',(1.,0.,0.));
#18729=DIRECTION('',(-0.707106781186547,0.707106781186548,-8.65956056235493E-17));
#18730=DIRECTION('center_axis',(0.,-1.,0.));
#18731=DIRECTION('ref_axis',(0.,0.,-1.));
#18732=DIRECTION('center_axis',(0.866025403784439,0.,-0.5));
#18733=DIRECTION('ref_axis',(0.5,0.,0.866025403784439));
#18734=DIRECTION('',(-0.5,0.,-0.866025403784439));
#18735=DIRECTION('',(0.,-1.,0.));
#18736=DIRECTION('',(0.5,0.,0.866025403784439));
#18737=DIRECTION('',(0.,-1.,0.));
#18738=DIRECTION('center_axis',(1.20185167898973E-16,0.,-1.));
#18739=DIRECTION('ref_axis',(1.,0.,1.20185167898973E-16));
#18740=DIRECTION('',(-1.,0.,-1.20185167898973E-16));
#18741=DIRECTION('',(0.,-1.,0.));
#18742=DIRECTION('',(1.,0.,1.20185167898973E-16));
#18743=DIRECTION('center_axis',(-0.866025403784439,0.,-0.5));
#18744=DIRECTION('ref_axis',(0.5,0.,-0.866025403784439));
#18745=DIRECTION('',(-0.5,0.,0.866025403784439));
#18746=DIRECTION('',(0.,-1.,0.));
#18747=DIRECTION('',(0.5,0.,-0.866025403784439));
#18748=DIRECTION('center_axis',(-0.866025403784439,0.,0.5));
#18749=DIRECTION('ref_axis',(-0.5,0.,-0.866025403784439));
#18750=DIRECTION('',(0.5,0.,0.866025403784439));
#18751=DIRECTION('',(0.,-1.,0.));
#18752=DIRECTION('',(-0.5,0.,-0.866025403784439));
#18753=DIRECTION('center_axis',(-2.40370335797945E-16,0.,1.));
#18754=DIRECTION('ref_axis',(-1.,0.,-2.40370335797945E-16));
#18755=DIRECTION('',(1.,0.,2.40370335797945E-16));
#18756=DIRECTION('',(0.,-1.,0.));
#18757=DIRECTION('',(-1.,0.,-2.40370335797945E-16));
#18758=DIRECTION('center_axis',(0.866025403784439,0.,0.5));
#18759=DIRECTION('ref_axis',(-0.5,0.,0.866025403784439));
#18760=DIRECTION('',(0.5,0.,-0.866025403784439));
#18761=DIRECTION('',(-0.5,0.,0.866025403784439));
#18762=DIRECTION('center_axis',(0.,1.,0.));
#18763=DIRECTION('ref_axis',(1.,0.,0.));
#18764=DIRECTION('center_axis',(0.,-1.,0.));
#18765=DIRECTION('ref_axis',(0.,0.,-1.));
#23585=CARTESIAN_POINT('',(0.,0.,0.));
#23586=CARTESIAN_POINT('Origin',(0.375,0.5,0.));
#23587=CARTESIAN_POINT('',(-0.375,0.5,-4.59242549680257E-17));
#23588=CARTESIAN_POINT('Origin',(0.,0.5,0.));
#23589=CARTESIAN_POINT('Origin',(0.,0.475,0.));
#23590=CARTESIAN_POINT('',(-0.425,0.45,-5.20474889637625E-17));
#23591=CARTESIAN_POINT('Origin',(0.,0.45,0.));
#23592=CARTESIAN_POINT('',(-0.4,0.475,-4.89858719658941E-17));
#23593=CARTESIAN_POINT('Origin',(0.,0.24,0.));
#23594=CARTESIAN_POINT('',(-0.425,0.0299999999999998,-5.20474889637625E-17));
#23595=CARTESIAN_POINT('Origin',(0.,0.0299999999999998,0.));
#23596=CARTESIAN_POINT('',(-0.425,0.24,-5.20474889637625E-17));
#23597=CARTESIAN_POINT('Origin',(0.,0.0150000000000001,0.));
#23598=CARTESIAN_POINT('',(-0.395,4.85722573273506E-17,-4.83735485663204E-17));
#23599=CARTESIAN_POINT('Origin',(0.,0.,0.));
#23600=CARTESIAN_POINT('',(-0.41,0.0150000000000001,-5.02105187650415E-17));
#23601=CARTESIAN_POINT('Origin',(0.27,0.,0.));
#23602=CARTESIAN_POINT('',(-0.27,0.,-3.30654635769785E-17));
#23603=CARTESIAN_POINT('Origin',(0.,0.,0.));
#23604=CARTESIAN_POINT('Origin',(0.,-0.02,0.));
#23605=CARTESIAN_POINT('',(-0.24505,-0.0498999999999999,3.00099698131059E-17));
#23606=CARTESIAN_POINT('Origin',(0.,-0.0498999999999999,0.));
#23607=CARTESIAN_POINT('',(-0.26,-0.02,-3.18408167778312E-17));
#23608=CARTESIAN_POINT('Origin',(0.,-0.995,0.));
#23609=CARTESIAN_POINT('',(-0.24505,-1.95495,3.00099698131059E-17));
#23610=CARTESIAN_POINT('Origin',(0.,-1.95495,0.));
#23611=CARTESIAN_POINT('',(-0.24505,-0.995,-3.00099698131059E-17));
#23612=CARTESIAN_POINT('Origin',(0.,-1.975,0.));
#23613=CARTESIAN_POINT('',(-0.2,-2.,-2.44929359829471E-17));
#23614=CARTESIAN_POINT('Origin',(0.,-2.,0.));
#23615=CARTESIAN_POINT('',(-0.225,-1.975,-2.75545529808154E-17));
#23616=CARTESIAN_POINT('Origin',(0.,-2.,0.));
#23617=CARTESIAN_POINT('Origin',(0.115470053837925,-0.5,-0.2));
#23618=CARTESIAN_POINT('',(0.23094010767585,-0.5,0.));
#23619=CARTESIAN_POINT('',(0.115470053837925,-0.5,-0.2));
#23620=CARTESIAN_POINT('',(0.23094010767585,-0.5,0.));
#23621=CARTESIAN_POINT('',(0.115470053837925,-0.8,-0.2));
#23622=CARTESIAN_POINT('',(0.115470053837925,-0.5,-0.2));
#23623=CARTESIAN_POINT('',(0.23094010767585,-0.8,0.));
#23624=CARTESIAN_POINT('',(0.23094010767585,-0.8,0.));
#23625=CARTESIAN_POINT('',(0.23094010767585,-0.5,0.));
#23626=CARTESIAN_POINT('Origin',(-0.115470053837925,-0.5,-0.2));
#23627=CARTESIAN_POINT('',(-0.115470053837925,-0.5,-0.2));
#23628=CARTESIAN_POINT('',(0.115470053837925,-0.5,-0.2));
#23629=CARTESIAN_POINT('',(-0.115470053837925,-0.8,-0.2));
#23630=CARTESIAN_POINT('',(-0.115470053837925,-0.5,-0.2));
#23631=CARTESIAN_POINT('',(0.115470053837925,-0.8,-0.2));
#23632=CARTESIAN_POINT('Origin',(-0.23094010767585,-0.5,-2.77555756156289E-17));
#23633=CARTESIAN_POINT('',(-0.23094010767585,-0.5,-2.82820063659975E-17));
#23634=CARTESIAN_POINT('',(-0.115470053837925,-0.5,-0.2));
#23635=CARTESIAN_POINT('',(-0.23094010767585,-0.8,-2.77555756156289E-17));
#23636=CARTESIAN_POINT('',(-0.23094010767585,-0.5,-2.82820063659975E-17));
#23637=CARTESIAN_POINT('',(-0.115470053837925,-0.8,-0.2));
#23638=CARTESIAN_POINT('Origin',(-0.115470053837925,-0.5,0.2));
#23639=CARTESIAN_POINT('',(-0.115470053837925,-0.5,0.2));
#23640=CARTESIAN_POINT('',(-0.23094010767585,-0.5,-2.82820063659975E-17));
#23641=CARTESIAN_POINT('',(-0.115470053837925,-0.8,0.2));
#23642=CARTESIAN_POINT('',(-0.115470053837925,-0.5,0.2));
#23643=CARTESIAN_POINT('',(-0.23094010767585,-0.8,-2.82820063659975E-17));
#23644=CARTESIAN_POINT('Origin',(0.115470053837925,-0.5,0.2));
#23645=CARTESIAN_POINT('',(0.115470053837925,-0.5,0.2));
#23646=CARTESIAN_POINT('',(-0.115470053837925,-0.5,0.2));
#23647=CARTESIAN_POINT('',(0.115470053837925,-0.8,0.2));
#23648=CARTESIAN_POINT('',(0.115470053837925,-0.5,0.2));
#23649=CARTESIAN_POINT('',(-0.115470053837925,-0.8,0.2));
#23650=CARTESIAN_POINT('Origin',(0.23094010767585,-0.5,0.));
#23651=CARTESIAN_POINT('',(0.115470053837925,-0.5,0.2));
#23652=CARTESIAN_POINT('',(0.115470053837925,-0.8,0.2));
#23653=CARTESIAN_POINT('Origin',(0.,-0.5,0.));
#23654=CARTESIAN_POINT('Origin',(0.,-0.8,0.));
#26958=UNCERTAINTY_MEASURE_WITH_UNIT(LENGTH_MEASURE(0.001),#27070,
'DISTANCE_ACCURACY_VALUE',
'Maximum model space distance between geometric entities at asserted c
onnectivities');
#26992=UNCERTAINTY_MEASURE_WITH_UNIT(LENGTH_MEASURE(0.001),#27070,
'DISTANCE_ACCURACY_VALUE',
'Maximum model space distance between geometric entities at asserted c
onnectivities');
#27035=(
GEOMETRIC_REPRESENTATION_CONTEXT(3)
GLOBAL_UNCERTAINTY_ASSIGNED_CONTEXT((#26958))
GLOBAL_UNIT_ASSIGNED_CONTEXT((#27070,#27072,#27073))
REPRESENTATION_CONTEXT('','3D')
);
#27069=(
GEOMETRIC_REPRESENTATION_CONTEXT(3)
GLOBAL_UNCERTAINTY_ASSIGNED_CONTEXT((#26992))
GLOBAL_UNIT_ASSIGNED_CONTEXT((#27070,#27072,#27073))
REPRESENTATION_CONTEXT('','3D')
);
#27070=(
LENGTH_UNIT()
NAMED_UNIT(*)
SI_UNIT(.CENTI.,.METRE.)
);
#27072=(
NAMED_UNIT(*)
PLANE_ANGLE_UNIT()
SI_UNIT($,.RADIAN.)
);
#27073=(
NAMED_UNIT(*)
SI_UNIT($,.STERADIAN.)
SOLID_ANGLE_UNIT()
);
#27116=SHAPE_DEFINITION_REPRESENTATION(#27202,#27393);
#27202=PRODUCT_DEFINITION_SHAPE('',$,#27470);
#27393=SHAPE_REPRESENTATION('',(#15481),#27035);
#27427=PRODUCT_DEFINITION_CONTEXT('part definition',#27657,'design');
#27470=PRODUCT_DEFINITION('Cap Screw - M5x20','Cap Screw - M5x20',#27546,
#27427);
#27546=PRODUCT_DEFINITION_FORMATION('',$,#27701);
#27657=APPLICATION_CONTEXT(
'Core Data for Automotive Mechanical Design Process');
#27658=PRODUCT_CONTEXT('part definition',#27657,'mechanical');
#27701=PRODUCT('Cap Screw - M5x20','Cap Screw - M5x20',
'Cap Screw - M5x20',(#27658));
#27798=COLOUR_RGB('Black',0.12,0.14,0.17);
#27799=FILL_AREA_STYLE_COLOUR('',#27798);
#27800=FILL_AREA_STYLE('',(#27799));
#27801=SURFACE_STYLE_FILL_AREA(#27800);
#27802=SURFACE_SIDE_STYLE('',(#27801));
#27803=SURFACE_STYLE_USAGE(.BOTH.,#27802);
#27804=PRESENTATION_STYLE_ASSIGNMENT((#27803));
ENDSEC;
END-ISO-10303-21;
